ISO-10303-21;
HEADER;
/* Generated by software containing ST-Developer
 * from STEP Tools, Inc. (www.steptools.com) 
 */

FILE_DESCRIPTION(
/* description */ ('PAT-001'),
/* implementation_level */ '2;1');

FILE_NAME(
/* name */ 'Bearing insert (1).step',
/* time_stamp */ '2026-10-29T17:07:15-07:00',
/* author */ (''),
/* organization */ (''),
/* preprocessor_version */ 'ST-DEVELOPER v20.2',
/* originating_system */ 'Autodesk Translation Framework v15.17.0.0',
/* authorisation */ '');

FILE_SCHEMA (('AUTOMOTIVE_DESIGN { 1 0 10303 214 3 1 1 }'));
ENDSEC;

DATA;
#10=MECHANICAL_DESIGN_GEOMETRIC_PRESENTATION_REPRESENTATION('',(#402),#9622);
#344=SHAPE_REPRESENTATION_RELATIONSHIP('SRR','None',#9769,#369);
#369=ADVANCED_BREP_SHAPE_REPRESENTATION('',(#434),#9618);
#402=STYLED_ITEM('',(#9962),#434);
#434=MANIFOLD_SOLID_BREP('Body1',#5228);
#504=FACE_BOUND('',#1341,.T.);
#505=FACE_BOUND('',#1345,.T.);
#506=FACE_BOUND('',#1346,.T.);
#507=FACE_BOUND('',#1347,.T.);
#508=FACE_BOUND('',#1348,.T.);
#509=FACE_BOUND('',#1349,.T.);
#510=FACE_BOUND('',#1351,.T.);
#511=FACE_BOUND('',#1352,.T.);
#512=FACE_BOUND('',#1353,.T.);
#513=FACE_BOUND('',#1354,.T.);
#514=FACE_BOUND('',#1355,.T.);
#697=PLANE('',#5988);
#698=PLANE('',#5995);
#699=PLANE('',#5996);
#972=FACE_OUTER_BOUND('',#1335,.T.);
#973=FACE_OUTER_BOUND('',#1336,.T.);
#974=FACE_OUTER_BOUND('',#1337,.T.);
#975=FACE_OUTER_BOUND('',#1338,.T.);
#976=FACE_OUTER_BOUND('',#1339,.T.);
#977=FACE_OUTER_BOUND('',#1340,.T.);
#978=FACE_OUTER_BOUND('',#1342,.T.);
#979=FACE_OUTER_BOUND('',#1343,.T.);
#980=FACE_OUTER_BOUND('',#1344,.T.);
#981=FACE_OUTER_BOUND('',#1350,.T.);
#1335=EDGE_LOOP('',(#4673,#4674,#4675,#4676));
#1336=EDGE_LOOP('',(#4677,#4678,#4679,#4680));
#1337=EDGE_LOOP('',(#4681,#4682,#4683,#4684));
#1338=EDGE_LOOP('',(#4685,#4686,#4687,#4688));
#1339=EDGE_LOOP('',(#4689,#4690,#4691,#4692));
#1340=EDGE_LOOP('',(#4693));
#1341=EDGE_LOOP('',(#4694));
#1342=EDGE_LOOP('',(#4695,#4696,#4697,#4698));
#1343=EDGE_LOOP('',(#4699,#4700,#4701,#4702));
#1344=EDGE_LOOP('',(#4703));
#1345=EDGE_LOOP('',(#4704));
#1346=EDGE_LOOP('',(#4705));
#1347=EDGE_LOOP('',(#4706));
#1348=EDGE_LOOP('',(#4707));
#1349=EDGE_LOOP('',(#4708));
#1350=EDGE_LOOP('',(#4709));
#1351=EDGE_LOOP('',(#4710));
#1352=EDGE_LOOP('',(#4711));
#1353=EDGE_LOOP('',(#4712));
#1354=EDGE_LOOP('',(#4713));
#1355=EDGE_LOOP('',(#4714));
#1764=LINE('',#9344,#2169);
#1765=LINE('',#9350,#2170);
#1766=LINE('',#9356,#2171);
#1767=LINE('',#9362,#2172);
#1768=LINE('',#9368,#2173);
#1769=LINE('',#9376,#2174);
#1770=LINE('',#9381,#2175);
#2169=VECTOR('',#7405,0.165);
#2170=VECTOR('',#7412,0.165);
#2171=VECTOR('',#7419,0.165);
#2172=VECTOR('',#7426,0.165);
#2173=VECTOR('',#7433,1.2);
#2174=VECTOR('',#7444,1.5);
#2175=VECTOR('',#7449,2.2);
#2382=CIRCLE('',#5974,0.165);
#2383=CIRCLE('',#5975,0.165);
#2384=CIRCLE('',#5977,0.165);
#2385=CIRCLE('',#5978,0.165);
#2386=CIRCLE('',#5980,0.165);
#2387=CIRCLE('',#5981,0.165);
#2388=CIRCLE('',#5983,0.165);
#2389=CIRCLE('',#5984,0.165);
#2390=CIRCLE('',#5986,1.2);
#2391=CIRCLE('',#5987,1.2);
#2392=CIRCLE('',#5989,1.5);
#2393=CIRCLE('',#5991,1.5);
#2394=CIRCLE('',#5993,2.2);
#2395=CIRCLE('',#5994,2.2);
#2812=VERTEX_POINT('',#9341);
#2813=VERTEX_POINT('',#9343);
#2814=VERTEX_POINT('',#9347);
#2815=VERTEX_POINT('',#9349);
#2816=VERTEX_POINT('',#9353);
#2817=VERTEX_POINT('',#9355);
#2818=VERTEX_POINT('',#9359);
#2819=VERTEX_POINT('',#9361);
#2820=VERTEX_POINT('',#9365);
#2821=VERTEX_POINT('',#9367);
#2822=VERTEX_POINT('',#9371);
#2823=VERTEX_POINT('',#9374);
#2824=VERTEX_POINT('',#9378);
#2825=VERTEX_POINT('',#9380);
#3440=EDGE_CURVE('',#2812,#2812,#2382,.T.);
#3441=EDGE_CURVE('',#2812,#2813,#1764,.T.);
#3442=EDGE_CURVE('',#2813,#2813,#2383,.T.);
#3443=EDGE_CURVE('',#2814,#2814,#2384,.T.);
#3444=EDGE_CURVE('',#2814,#2815,#1765,.T.);
#3445=EDGE_CURVE('',#2815,#2815,#2385,.T.);
#3446=EDGE_CURVE('',#2816,#2816,#2386,.T.);
#3447=EDGE_CURVE('',#2816,#2817,#1766,.T.);
#3448=EDGE_CURVE('',#2817,#2817,#2387,.T.);
#3449=EDGE_CURVE('',#2818,#2818,#2388,.T.);
#3450=EDGE_CURVE('',#2818,#2819,#1767,.T.);
#3451=EDGE_CURVE('',#2819,#2819,#2389,.T.);
#3452=EDGE_CURVE('',#2820,#2820,#2390,.T.);
#3453=EDGE_CURVE('',#2820,#2821,#1768,.T.);
#3454=EDGE_CURVE('',#2821,#2821,#2391,.T.);
#3455=EDGE_CURVE('',#2822,#2822,#2392,.T.);
#3456=EDGE_CURVE('',#2823,#2823,#2393,.T.);
#3457=EDGE_CURVE('',#2823,#2822,#1769,.T.);
#3458=EDGE_CURVE('',#2824,#2824,#2394,.T.);
#3459=EDGE_CURVE('',#2824,#2825,#1770,.T.);
#3460=EDGE_CURVE('',#2825,#2825,#2395,.T.);
#4673=ORIENTED_EDGE('',*,*,#3440,.F.);
#4674=ORIENTED_EDGE('',*,*,#3441,.T.);
#4675=ORIENTED_EDGE('',*,*,#3442,.F.);
#4676=ORIENTED_EDGE('',*,*,#3441,.F.);
#4677=ORIENTED_EDGE('',*,*,#3443,.F.);
#4678=ORIENTED_EDGE('',*,*,#3444,.T.);
#4679=ORIENTED_EDGE('',*,*,#3445,.F.);
#4680=ORIENTED_EDGE('',*,*,#3444,.F.);
#4681=ORIENTED_EDGE('',*,*,#3446,.F.);
#4682=ORIENTED_EDGE('',*,*,#3447,.T.);
#4683=ORIENTED_EDGE('',*,*,#3448,.F.);
#4684=ORIENTED_EDGE('',*,*,#3447,.F.);
#4685=ORIENTED_EDGE('',*,*,#3449,.F.);
#4686=ORIENTED_EDGE('',*,*,#3450,.T.);
#4687=ORIENTED_EDGE('',*,*,#3451,.F.);
#4688=ORIENTED_EDGE('',*,*,#3450,.F.);
#4689=ORIENTED_EDGE('',*,*,#3452,.F.);
#4690=ORIENTED_EDGE('',*,*,#3453,.T.);
#4691=ORIENTED_EDGE('',*,*,#3454,.T.);
#4692=ORIENTED_EDGE('',*,*,#3453,.F.);
#4693=ORIENTED_EDGE('',*,*,#3455,.F.);
#4694=ORIENTED_EDGE('',*,*,#3452,.T.);
#4695=ORIENTED_EDGE('',*,*,#3456,.F.);
#4696=ORIENTED_EDGE('',*,*,#3457,.T.);
#4697=ORIENTED_EDGE('',*,*,#3455,.T.);
#4698=ORIENTED_EDGE('',*,*,#3457,.F.);
#4699=ORIENTED_EDGE('',*,*,#3458,.F.);
#4700=ORIENTED_EDGE('',*,*,#3459,.T.);
#4701=ORIENTED_EDGE('',*,*,#3460,.T.);
#4702=ORIENTED_EDGE('',*,*,#3459,.F.);
#4703=ORIENTED_EDGE('',*,*,#3458,.T.);
#4704=ORIENTED_EDGE('',*,*,#3456,.T.);
#4705=ORIENTED_EDGE('',*,*,#3451,.T.);
#4706=ORIENTED_EDGE('',*,*,#3448,.T.);
#4707=ORIENTED_EDGE('',*,*,#3445,.T.);
#4708=ORIENTED_EDGE('',*,*,#3442,.T.);
#4709=ORIENTED_EDGE('',*,*,#3460,.F.);
#4710=ORIENTED_EDGE('',*,*,#3454,.F.);
#4711=ORIENTED_EDGE('',*,*,#3449,.T.);
#4712=ORIENTED_EDGE('',*,*,#3446,.T.);
#4713=ORIENTED_EDGE('',*,*,#3443,.T.);
#4714=ORIENTED_EDGE('',*,*,#3440,.T.);
#4885=CYLINDRICAL_SURFACE('',#5973,0.165);
#4886=CYLINDRICAL_SURFACE('',#5976,0.165);
#4887=CYLINDRICAL_SURFACE('',#5979,0.165);
#4888=CYLINDRICAL_SURFACE('',#5982,0.165);
#4889=CYLINDRICAL_SURFACE('',#5985,1.2);
#4890=CYLINDRICAL_SURFACE('',#5990,1.5);
#4891=CYLINDRICAL_SURFACE('',#5992,2.2);
#5159=ADVANCED_FACE('',(#972),#4885,.F.);
#5160=ADVANCED_FACE('',(#973),#4886,.F.);
#5161=ADVANCED_FACE('',(#974),#4887,.F.);
#5162=ADVANCED_FACE('',(#975),#4888,.F.);
#5163=ADVANCED_FACE('',(#976),#4889,.F.);
#5164=ADVANCED_FACE('',(#977,#504),#697,.T.);
#5165=ADVANCED_FACE('',(#978),#4890,.F.);
#5166=ADVANCED_FACE('',(#979),#4891,.T.);
#5167=ADVANCED_FACE('',(#980,#505,#506,#507,#508,#509),#698,.T.);
#5168=ADVANCED_FACE('',(#981,#510,#511,#512,#513,#514),#699,.F.);
#5228=CLOSED_SHELL('',(#5159,#5160,#5161,#5162,#5163,#5164,#5165,#5166,
#5167,#5168));
#5972=AXIS2_PLACEMENT_3D('',#9339,#7399,#7400);
#5973=AXIS2_PLACEMENT_3D('',#9340,#7401,#7402);
#5974=AXIS2_PLACEMENT_3D('',#9342,#7403,#7404);
#5975=AXIS2_PLACEMENT_3D('',#9345,#7406,#7407);
#5976=AXIS2_PLACEMENT_3D('',#9346,#7408,#7409);
#5977=AXIS2_PLACEMENT_3D('',#9348,#7410,#7411);
#5978=AXIS2_PLACEMENT_3D('',#9351,#7413,#7414);
#5979=AXIS2_PLACEMENT_3D('',#9352,#7415,#7416);
#5980=AXIS2_PLACEMENT_3D('',#9354,#7417,#7418);
#5981=AXIS2_PLACEMENT_3D('',#9357,#7420,#7421);
#5982=AXIS2_PLACEMENT_3D('',#9358,#7422,#7423);
#5983=AXIS2_PLACEMENT_3D('',#9360,#7424,#7425);
#5984=AXIS2_PLACEMENT_3D('',#9363,#7427,#7428);
#5985=AXIS2_PLACEMENT_3D('',#9364,#7429,#7430);
#5986=AXIS2_PLACEMENT_3D('',#9366,#7431,#7432);
#5987=AXIS2_PLACEMENT_3D('',#9369,#7434,#7435);
#5988=AXIS2_PLACEMENT_3D('',#9370,#7436,#7437);
#5989=AXIS2_PLACEMENT_3D('',#9372,#7438,#7439);
#5990=AXIS2_PLACEMENT_3D('',#9373,#7440,#7441);
#5991=AXIS2_PLACEMENT_3D('',#9375,#7442,#7443);
#5992=AXIS2_PLACEMENT_3D('',#9377,#7445,#7446);
#5993=AXIS2_PLACEMENT_3D('',#9379,#7447,#7448);
#5994=AXIS2_PLACEMENT_3D('',#9382,#7450,#7451);
#5995=AXIS2_PLACEMENT_3D('',#9383,#7452,#7453);
#5996=AXIS2_PLACEMENT_3D('',#9384,#7454,#7455);
#7399=DIRECTION('axis',(0.,0.,1.));
#7400=DIRECTION('refdir',(1.,0.,0.));
#7401=DIRECTION('center_axis',(0.,1.,0.));
#7402=DIRECTION('ref_axis',(1.,0.,0.));
#7403=DIRECTION('center_axis',(0.,1.,0.));
#7404=DIRECTION('ref_axis',(1.,0.,0.));
#7405=DIRECTION('',(0.,1.,0.));
#7406=DIRECTION('center_axis',(0.,-1.,0.));
#7407=DIRECTION('ref_axis',(1.,0.,0.));
#7408=DIRECTION('center_axis',(0.,1.,0.));
#7409=DIRECTION('ref_axis',(1.,0.,0.));
#7410=DIRECTION('center_axis',(0.,1.,0.));
#7411=DIRECTION('ref_axis',(1.,0.,0.));
#7412=DIRECTION('',(0.,1.,0.));
#7413=DIRECTION('center_axis',(0.,-1.,0.));
#7414=DIRECTION('ref_axis',(1.,0.,0.));
#7415=DIRECTION('center_axis',(0.,1.,0.));
#7416=DIRECTION('ref_axis',(1.,0.,0.));
#7417=DIRECTION('center_axis',(0.,1.,0.));
#7418=DIRECTION('ref_axis',(1.,0.,0.));
#7419=DIRECTION('',(0.,1.,0.));
#7420=DIRECTION('center_axis',(0.,-1.,0.));
#7421=DIRECTION('ref_axis',(1.,0.,0.));
#7422=DIRECTION('center_axis',(0.,1.,0.));
#7423=DIRECTION('ref_axis',(1.,0.,0.));
#7424=DIRECTION('center_axis',(0.,1.,0.));
#7425=DIRECTION('ref_axis',(1.,0.,0.));
#7426=DIRECTION('',(0.,1.,0.));
#7427=DIRECTION('center_axis',(0.,-1.,0.));
#7428=DIRECTION('ref_axis',(1.,0.,0.));
#7429=DIRECTION('center_axis',(0.,1.,0.));
#7430=DIRECTION('ref_axis',(1.,0.,0.));
#7431=DIRECTION('center_axis',(0.,-1.,0.));
#7432=DIRECTION('ref_axis',(1.,0.,0.));
#7433=DIRECTION('',(0.,-1.,0.));
#7434=DIRECTION('center_axis',(0.,-1.,0.));
#7435=DIRECTION('ref_axis',(1.,0.,0.));
#7436=DIRECTION('center_axis',(0.,1.,0.));
#7437=DIRECTION('ref_axis',(1.,0.,0.));
#7438=DIRECTION('center_axis',(0.,-1.,0.));
#7439=DIRECTION('ref_axis',(1.,0.,0.));
#7440=DIRECTION('center_axis',(0.,1.,0.));
#7441=DIRECTION('ref_axis',(1.,0.,0.));
#7442=DIRECTION('center_axis',(0.,-1.,0.));
#7443=DIRECTION('ref_axis',(1.,0.,0.));
#7444=DIRECTION('',(0.,-1.,0.));
#7445=DIRECTION('center_axis',(0.,1.,0.));
#7446=DIRECTION('ref_axis',(1.,0.,0.));
#7447=DIRECTION('center_axis',(0.,1.,0.));
#7448=DIRECTION('ref_axis',(1.,0.,0.));
#7449=DIRECTION('',(0.,-1.,0.));
#7450=DIRECTION('center_axis',(0.,1.,0.));
#7451=DIRECTION('ref_axis',(1.,0.,0.));
#7452=DIRECTION('center_axis',(0.,1.,0.));
#7453=DIRECTION('ref_axis',(1.,0.,0.));
#7454=DIRECTION('center_axis',(0.,1.,0.));
#7455=DIRECTION('ref_axis',(1.,0.,0.));
#9339=CARTESIAN_POINT('',(0.,0.,0.));
#9340=CARTESIAN_POINT('Origin',(-1.9,28.7,4.5));
#9341=CARTESIAN_POINT('',(-2.065,28.8,4.5));
#9342=CARTESIAN_POINT('Origin',(-1.9,28.8,4.5));
#9343=CARTESIAN_POINT('',(-2.065,30.,4.5));
#9344=CARTESIAN_POINT('',(-2.065,28.7,4.5));
#9345=CARTESIAN_POINT('Origin',(-1.9,30.,4.5));
#9346=CARTESIAN_POINT('Origin',(1.16341445918999E-16,28.7,6.4));
#9347=CARTESIAN_POINT('',(-0.165,28.8,6.4));
#9348=CARTESIAN_POINT('Origin',(1.16341445918999E-16,28.8,6.4));
#9349=CARTESIAN_POINT('',(-0.165,30.,6.4));
#9350=CARTESIAN_POINT('',(-0.165,28.7,6.4));
#9351=CARTESIAN_POINT('Origin',(1.16341445918999E-16,30.,6.4));
#9352=CARTESIAN_POINT('Origin',(1.9,28.7,4.5));
#9353=CARTESIAN_POINT('',(1.735,28.8,4.5));
#9354=CARTESIAN_POINT('Origin',(1.9,28.8,4.5));
#9355=CARTESIAN_POINT('',(1.735,30.,4.5));
#9356=CARTESIAN_POINT('',(1.735,28.7,4.5));
#9357=CARTESIAN_POINT('Origin',(1.9,30.,4.5));
#9358=CARTESIAN_POINT('Origin',(-3.49024337756996E-16,28.7,2.6));
#9359=CARTESIAN_POINT('',(-0.165,28.8,2.6));
#9360=CARTESIAN_POINT('Origin',(-3.49024337756996E-16,28.8,2.6));
#9361=CARTESIAN_POINT('',(-0.165,30.,2.6));
#9362=CARTESIAN_POINT('',(-0.165,28.7,2.6));
#9363=CARTESIAN_POINT('Origin',(-3.49024337756996E-16,30.,2.6));
#9364=CARTESIAN_POINT('Origin',(0.,28.8,4.5));
#9365=CARTESIAN_POINT('',(-1.2,29.1,4.5));
#9366=CARTESIAN_POINT('Origin',(0.,29.1,4.5));
#9367=CARTESIAN_POINT('',(-1.2,28.8,4.5));
#9368=CARTESIAN_POINT('',(-1.2,28.8,4.5));
#9369=CARTESIAN_POINT('Origin',(0.,28.8,4.5));
#9370=CARTESIAN_POINT('Origin',(0.,29.1,4.5));
#9371=CARTESIAN_POINT('',(-1.5,29.1,4.5));
#9372=CARTESIAN_POINT('Origin',(0.,29.1,4.5));
#9373=CARTESIAN_POINT('Origin',(0.,28.8,4.5));
#9374=CARTESIAN_POINT('',(-1.5,30.,4.5));
#9375=CARTESIAN_POINT('Origin',(0.,30.,4.5));
#9376=CARTESIAN_POINT('',(-1.5,28.8,4.5));
#9377=CARTESIAN_POINT('Origin',(0.,28.8,4.5));
#9378=CARTESIAN_POINT('',(-2.2,30.,4.5));
#9379=CARTESIAN_POINT('Origin',(0.,30.,4.5));
#9380=CARTESIAN_POINT('',(-2.2,28.8,4.5));
#9381=CARTESIAN_POINT('',(-2.2,28.8,4.5));
#9382=CARTESIAN_POINT('Origin',(0.,28.8,4.5));
#9383=CARTESIAN_POINT('Origin',(0.,30.,4.5));
#9384=CARTESIAN_POINT('Origin',(0.,28.8,4.5));
#9588=UNCERTAINTY_MEASURE_WITH_UNIT(LENGTH_MEASURE(0.001),#9623,
'DISTANCE_ACCURACY_VALUE',
'Maximum model space distance between geometric entities at asserted c
onnectivities');
#9592=UNCERTAINTY_MEASURE_WITH_UNIT(LENGTH_MEASURE(0.001),#9623,
'DISTANCE_ACCURACY_VALUE',
'Maximum model space distance between geometric entities at asserted c
onnectivities');
#9618=(
GEOMETRIC_REPRESENTATION_CONTEXT(3)
GLOBAL_UNCERTAINTY_ASSIGNED_CONTEXT((#9588))
GLOBAL_UNIT_ASSIGNED_CONTEXT((#9623,#9625,#9626))
REPRESENTATION_CONTEXT('','3D')
);
#9622=(
GEOMETRIC_REPRESENTATION_CONTEXT(3)
GLOBAL_UNCERTAINTY_ASSIGNED_CONTEXT((#9592))
GLOBAL_UNIT_ASSIGNED_CONTEXT((#9623,#9625,#9626))
REPRESENTATION_CONTEXT('','3D')
);
#9623=(
LENGTH_UNIT()
NAMED_UNIT(*)
SI_UNIT(.CENTI.,.METRE.)
);
#9625=(
NAMED_UNIT(*)
PLANE_ANGLE_UNIT()
SI_UNIT($,.RADIAN.)
);
#9626=(
NAMED_UNIT(*)
SI_UNIT($,.STERADIAN.)
SOLID_ANGLE_UNIT()
);
#9652=SHAPE_DEFINITION_REPRESENTATION(#9686,#9769);
#9686=PRODUCT_DEFINITION_SHAPE('',$,#9799);
#9769=SHAPE_REPRESENTATION('',(#5972),#9618);
#9773=PRODUCT_DEFINITION_CONTEXT('part definition',#9862,'design');
#9799=PRODUCT_DEFINITION('Bearing insert (1)','Bearing insert (1)',#9828,
#9773);
#9828=PRODUCT_DEFINITION_FORMATION('',$,#9889);
#9862=APPLICATION_CONTEXT(
'Core Data for Automotive Mechanical Design Process');
#9863=PRODUCT_CONTEXT('part definition',#9862,'mechanical');
#9889=PRODUCT('Bearing insert (1)','Bearing insert (1)','Bearing insert (1)',
(#9863));
#9956=COLOUR_RGB('Grey',0.48,0.52,0.57);
#9957=FILL_AREA_STYLE_COLOUR('',#9956);
#9958=FILL_AREA_STYLE('',(#9957));
#9959=SURFACE_STYLE_FILL_AREA(#9958);
#9960=SURFACE_SIDE_STYLE('',(#9959));
#9961=SURFACE_STYLE_USAGE(.BOTH.,#9960);
#9962=PRESENTATION_STYLE_ASSIGNMENT((#9961));
ENDSEC;
END-ISO-10303-21;
